ISO-10303-21;
HEADER;
/* Generated by software containing ST-Developer
 * from STEP Tools, Inc. (www.steptools.com) 
 */

FILE_DESCRIPTION(
/* description */ ('Ball-type isolation valve (generic)'),
/* implementation_level */ '2;1');

FILE_NAME(
/* name */ 'Bridge spacer (2).step',
/* time_stamp */ '2026-10-27T10:53:05-07:00',
/* author */ (''),
/* organization */ (''),
/* preprocessor_version */ 'ST-DEVELOPER v20.2',
/* originating_system */ 'Autodesk Translation Framework v15.17.0.0',
/* authorisation */ '');

FILE_SCHEMA (('AUTOMOTIVE_DESIGN { 1 0 10303 214 3 1 1 }'));
ENDSEC;

DATA;
#10=MECHANICAL_DESIGN_GEOMETRIC_PRESENTATION_REPRESENTATION('',(#288),#7425);
#236=SHAPE_REPRESENTATION_RELATIONSHIP('SRR','None',#7546,#262);
#262=ADVANCED_BREP_SHAPE_REPRESENTATION('',(#314),#7409);
#288=STYLED_ITEM('',(#7737),#314);
#314=MANIFOLD_SOLID_BREP('Body1',#4093);
#395=FACE_BOUND('',#999,.T.);
#396=FACE_BOUND('',#1001,.T.);
#474=PLANE('',#4620);
#475=PLANE('',#4621);
#683=FACE_OUTER_BOUND('',#996,.T.);
#684=FACE_OUTER_BOUND('',#997,.T.);
#685=FACE_OUTER_BOUND('',#998,.T.);
#686=FACE_OUTER_BOUND('',#1000,.T.);
#996=EDGE_LOOP('',(#3201,#3202,#3203,#3204));
#997=EDGE_LOOP('',(#3205,#3206,#3207,#3208));
#998=EDGE_LOOP('',(#3209));
#999=EDGE_LOOP('',(#3210));
#1000=EDGE_LOOP('',(#3211));
#1001=EDGE_LOOP('',(#3212));
#1280=LINE('',#6678,#1588);
#1281=LINE('',#6684,#1589);
#1588=VECTOR('',#5447,0.225);
#1589=VECTOR('',#5454,0.4);
#1879=CIRCLE('',#4615,0.225);
#1880=CIRCLE('',#4616,0.225);
#1881=CIRCLE('',#4618,0.4);
#1882=CIRCLE('',#4619,0.4);
#2099=VERTEX_POINT('',#6675);
#2100=VERTEX_POINT('',#6677);
#2101=VERTEX_POINT('',#6681);
#2102=VERTEX_POINT('',#6683);
#2493=EDGE_CURVE('',#2099,#2099,#1879,.T.);
#2494=EDGE_CURVE('',#2099,#2100,#1280,.T.);
#2495=EDGE_CURVE('',#2100,#2100,#1880,.T.);
#2496=EDGE_CURVE('',#2101,#2101,#1881,.T.);
#2497=EDGE_CURVE('',#2101,#2102,#1281,.T.);
#2498=EDGE_CURVE('',#2102,#2102,#1882,.T.);
#3201=ORIENTED_EDGE('',*,*,#2493,.F.);
#3202=ORIENTED_EDGE('',*,*,#2494,.T.);
#3203=ORIENTED_EDGE('',*,*,#2495,.T.);
#3204=ORIENTED_EDGE('',*,*,#2494,.F.);
#3205=ORIENTED_EDGE('',*,*,#2496,.F.);
#3206=ORIENTED_EDGE('',*,*,#2497,.T.);
#3207=ORIENTED_EDGE('',*,*,#2498,.T.);
#3208=ORIENTED_EDGE('',*,*,#2497,.F.);
#3209=ORIENTED_EDGE('',*,*,#2496,.T.);
#3210=ORIENTED_EDGE('',*,*,#2493,.T.);
#3211=ORIENTED_EDGE('',*,*,#2498,.F.);
#3212=ORIENTED_EDGE('',*,*,#2495,.F.);
#3809=CYLINDRICAL_SURFACE('',#4614,0.225);
#3810=CYLINDRICAL_SURFACE('',#4617,0.4);
#3937=ADVANCED_FACE('',(#683),#3809,.F.);
#3938=ADVANCED_FACE('',(#684),#3810,.T.);
#3939=ADVANCED_FACE('',(#685,#395),#474,.T.);
#3940=ADVANCED_FACE('',(#686,#396),#475,.F.);
#4093=CLOSED_SHELL('',(#3937,#3938,#3939,#3940));
#4613=AXIS2_PLACEMENT_3D('',#6673,#5441,#5442);
#4614=AXIS2_PLACEMENT_3D('',#6674,#5443,#5444);
#4615=AXIS2_PLACEMENT_3D('',#6676,#5445,#5446);
#4616=AXIS2_PLACEMENT_3D('',#6679,#5448,#5449);
#4617=AXIS2_PLACEMENT_3D('',#6680,#5450,#5451);
#4618=AXIS2_PLACEMENT_3D('',#6682,#5452,#5453);
#4619=AXIS2_PLACEMENT_3D('',#6685,#5455,#5456);
#4620=AXIS2_PLACEMENT_3D('',#6686,#5457,#5458);
#4621=AXIS2_PLACEMENT_3D('',#6687,#5459,#5460);
#5441=DIRECTION('axis',(0.,0.,1.));
#5442=DIRECTION('refdir',(1.,0.,0.));
#5443=DIRECTION('center_axis',(0.,0.,1.));
#5444=DIRECTION('ref_axis',(1.,0.,0.));
#5445=DIRECTION('center_axis',(0.,0.,-1.));
#5446=DIRECTION('ref_axis',(1.,0.,0.));
#5447=DIRECTION('',(0.,0.,-1.));
#5448=DIRECTION('center_axis',(0.,0.,-1.));
#5449=DIRECTION('ref_axis',(1.,0.,0.));
#5450=DIRECTION('center_axis',(0.,0.,1.));
#5451=DIRECTION('ref_axis',(1.,0.,0.));
#5452=DIRECTION('center_axis',(0.,0.,1.));
#5453=DIRECTION('ref_axis',(1.,0.,0.));
#5454=DIRECTION('',(0.,0.,-1.));
#5455=DIRECTION('center_axis',(0.,0.,1.));
#5456=DIRECTION('ref_axis',(1.,0.,0.));
#5457=DIRECTION('center_axis',(0.,0.,1.));
#5458=DIRECTION('ref_axis',(1.,0.,0.));
#5459=DIRECTION('center_axis',(0.,0.,1.));
#5460=DIRECTION('ref_axis',(1.,0.,0.));
#6673=CARTESIAN_POINT('',(0.,0.,0.));
#6674=CARTESIAN_POINT('Origin',(1.3,-1.,7.5));
#6675=CARTESIAN_POINT('',(1.075,-1.,8.));
#6676=CARTESIAN_POINT('Origin',(1.3,-1.,8.));
#6677=CARTESIAN_POINT('',(1.075,-1.,7.5));
#6678=CARTESIAN_POINT('',(1.075,-1.,7.5));
#6679=CARTESIAN_POINT('Origin',(1.3,-1.,7.5));
#6680=CARTESIAN_POINT('Origin',(1.3,-1.,7.5));
#6681=CARTESIAN_POINT('',(0.9,-1.,8.));
#6682=CARTESIAN_POINT('Origin',(1.3,-1.,8.));
#6683=CARTESIAN_POINT('',(0.9,-1.,7.5));
#6684=CARTESIAN_POINT('',(0.9,-1.,7.5));
#6685=CARTESIAN_POINT('Origin',(1.3,-1.,7.5));
#6686=CARTESIAN_POINT('Origin',(1.3,-1.,8.));
#6687=CARTESIAN_POINT('Origin',(1.3,-1.,7.5));
#7379=UNCERTAINTY_MEASURE_WITH_UNIT(LENGTH_MEASURE(0.001),#7426,
'DISTANCE_ACCURACY_VALUE',
'Maximum model space distance between geometric entities at asserted c
onnectivities');
#7395=UNCERTAINTY_MEASURE_WITH_UNIT(LENGTH_MEASURE(0.001),#7426,
'DISTANCE_ACCURACY_VALUE',
'Maximum model space distance between geometric entities at asserted c
onnectivities');
#7409=(
GEOMETRIC_REPRESENTATION_CONTEXT(3)
GLOBAL_UNCERTAINTY_ASSIGNED_CONTEXT((#7379))
GLOBAL_UNIT_ASSIGNED_CONTEXT((#7426,#7428,#7429))
REPRESENTATION_CONTEXT('','3D')
);
#7425=(
GEOMETRIC_REPRESENTATION_CONTEXT(3)
GLOBAL_UNCERTAINTY_ASSIGNED_CONTEXT((#7395))
GLOBAL_UNIT_ASSIGNED_CONTEXT((#7426,#7428,#7429))
REPRESENTATION_CONTEXT('','3D')
);
#7426=(
LENGTH_UNIT()
NAMED_UNIT(*)
SI_UNIT(.CENTI.,.METRE.)
);
#7428=(
NAMED_UNIT(*)
PLANE_ANGLE_UNIT()
SI_UNIT($,.RADIAN.)
);
#7429=(
NAMED_UNIT(*)
SI_UNIT($,.STERADIAN.)
SOLID_ANGLE_UNIT()
);
#7443=SHAPE_DEFINITION_REPRESENTATION(#7472,#7546);
#7472=PRODUCT_DEFINITION_SHAPE('',$,#7576);
#7546=SHAPE_REPRESENTATION('',(#4613),#7409);
#7562=PRODUCT_DEFINITION_CONTEXT('part definition',#7651,'design');
#7576=PRODUCT_DEFINITION('Bridge spacer (2)','Bridge spacer (2)',#7605,#7562);
#7605=PRODUCT_DEFINITION_FORMATION('',$,#7666);
#7651=APPLICATION_CONTEXT(
'Core Data for Automotive Mechanical Design Process');
#7652=PRODUCT_CONTEXT('part definition',#7651,'mechanical');
#7666=PRODUCT('Bridge spacer (2)','Bridge spacer (2)','Bridge spacer (2)',(#7652));
#7731=COLOUR_RGB('Sky Blue',0.24,0.69,0.87);
#7732=FILL_AREA_STYLE_COLOUR('',#7731);
#7733=FILL_AREA_STYLE('',(#7732));
#7734=SURFACE_STYLE_FILL_AREA(#7733);
#7735=SURFACE_SIDE_STYLE('',(#7734));
#7736=SURFACE_STYLE_USAGE(.BOTH.,#7735);
#7737=PRESENTATION_STYLE_ASSIGNMENT((#7736));
ENDSEC;
END-ISO-10303-21;
